ISO-10303-21;
HEADER;
/* Generated by software containing ST-Developer
 * from STEP Tools, Inc. (www.steptools.com) 
 */

FILE_DESCRIPTION(
/* description */ ('Turntable on roller ring'),
/* implementation_level */ '2;1');

FILE_NAME(
/* name */ 'Inner ring (1).step',
/* time_stamp */ '2026-10-28T03:23:59-07:00',
/* author */ (''),
/* organization */ (''),
/* preprocessor_version */ 'ST-DEVELOPER v20.2',
/* originating_system */ 'Autodesk Translation Framework v15.17.0.0',
/* authorisation */ '');

FILE_SCHEMA (('AUTOMOTIVE_DESIGN { 1 0 10303 214 3 1 1 }'));
ENDSEC;

DATA;
#10=MECHANICAL_DESIGN_GEOMETRIC_PRESENTATION_REPRESENTATION('',(#676),#16281);
#474=TOROIDAL_SURFACE('',#10042,1.,0.247676);
#495=CONICAL_SURFACE('',#10053,0.53,0.785398163397448);
#496=CONICAL_SURFACE('',#10060,0.53,0.785398163397448);
#557=SHAPE_REPRESENTATION_RELATIONSHIP('SRR','None',#16582,#612);
#612=ADVANCED_BREP_SHAPE_REPRESENTATION('',(#744),#16276);
#676=STYLED_ITEM('',(#16932),#744);
#744=MANIFOLD_SOLID_BREP('Body1',#8421);
#981=FACE_BOUND('',#2438,.T.);
#982=FACE_BOUND('',#2441,.T.);
#1233=PLANE('',#10055);
#1234=PLANE('',#10058);
#1704=FACE_OUTER_BOUND('',#2433,.T.);
#1705=FACE_OUTER_BOUND('',#2434,.T.);
#1706=FACE_OUTER_BOUND('',#2435,.T.);
#1707=FACE_OUTER_BOUND('',#2436,.T.);
#1708=FACE_OUTER_BOUND('',#2437,.T.);
#1709=FACE_OUTER_BOUND('',#2439,.T.);
#1710=FACE_OUTER_BOUND('',#2440,.T.);
#1711=FACE_OUTER_BOUND('',#2442,.T.);
#2433=EDGE_LOOP('',(#7457,#7458,#7459,#7460,#7461,#7462));
#2434=EDGE_LOOP('',(#7463,#7464,#7465,#7466,#7467));
#2435=EDGE_LOOP('',(#7468,#7469,#7470,#7471));
#2436=EDGE_LOOP('',(#7472,#7473,#7474,#7475));
#2437=EDGE_LOOP('',(#7476));
#2438=EDGE_LOOP('',(#7477));
#2439=EDGE_LOOP('',(#7478,#7479,#7480,#7481,#7482));
#2440=EDGE_LOOP('',(#7483));
#2441=EDGE_LOOP('',(#7484));
#2442=EDGE_LOOP('',(#7485,#7486,#7487,#7488));
#2960=LINE('',#15546,#3443);
#2961=LINE('',#15552,#3444);
#2962=LINE('',#15556,#3445);
#2963=LINE('',#15562,#3446);
#2964=LINE('',#15567,#3447);
#3443=VECTOR('',#12685,0.976185);
#3444=VECTOR('',#12692,0.5);
#3445=VECTOR('',#12697,0.53);
#3446=VECTOR('',#12706,0.976185);
#3447=VECTOR('',#12713,0.53);
#3877=CIRCLE('',#10043,0.976185);
#3878=CIRCLE('',#10044,0.976185);
#3879=CIRCLE('',#10045,0.247676);
#3880=CIRCLE('',#10046,0.976185);
#3881=CIRCLE('',#10047,0.976185);
#3882=CIRCLE('',#10049,0.976185);
#3883=CIRCLE('',#10051,0.5);
#3884=CIRCLE('',#10052,0.5);
#3885=CIRCLE('',#10054,0.56);
#3886=CIRCLE('',#10057,0.976185);
#3887=CIRCLE('',#10059,0.56);
#4553=VERTEX_POINT('',#15535);
#4554=VERTEX_POINT('',#15536);
#4555=VERTEX_POINT('',#15539);
#4556=VERTEX_POINT('',#15541);
#4557=VERTEX_POINT('',#15545);
#4558=VERTEX_POINT('',#15549);
#4559=VERTEX_POINT('',#15551);
#4560=VERTEX_POINT('',#15555);
#4561=VERTEX_POINT('',#15560);
#4562=VERTEX_POINT('',#15564);
#5539=EDGE_CURVE('',#4553,#4554,#3877,.T.);
#5540=EDGE_CURVE('',#4554,#4553,#3878,.T.);
#5541=EDGE_CURVE('',#4554,#4555,#3879,.T.);
#5542=EDGE_CURVE('',#4556,#4555,#3880,.T.);
#5543=EDGE_CURVE('',#4555,#4556,#3881,.T.);
#5544=EDGE_CURVE('',#4556,#4557,#2960,.T.);
#5545=EDGE_CURVE('',#4557,#4557,#3882,.T.);
#5546=EDGE_CURVE('',#4558,#4558,#3883,.T.);
#5547=EDGE_CURVE('',#4558,#4559,#2961,.T.);
#5548=EDGE_CURVE('',#4559,#4559,#3884,.T.);
#5549=EDGE_CURVE('',#4559,#4560,#2962,.T.);
#5550=EDGE_CURVE('',#4560,#4560,#3885,.T.);
#5551=EDGE_CURVE('',#4561,#4561,#3886,.T.);
#5552=EDGE_CURVE('',#4561,#4553,#2963,.T.);
#5553=EDGE_CURVE('',#4562,#4562,#3887,.T.);
#5554=EDGE_CURVE('',#4562,#4558,#2964,.T.);
#7457=ORIENTED_EDGE('',*,*,#5539,.F.);
#7458=ORIENTED_EDGE('',*,*,#5540,.F.);
#7459=ORIENTED_EDGE('',*,*,#5541,.T.);
#7460=ORIENTED_EDGE('',*,*,#5542,.F.);
#7461=ORIENTED_EDGE('',*,*,#5543,.F.);
#7462=ORIENTED_EDGE('',*,*,#5541,.F.);
#7463=ORIENTED_EDGE('',*,*,#5542,.T.);
#7464=ORIENTED_EDGE('',*,*,#5543,.T.);
#7465=ORIENTED_EDGE('',*,*,#5544,.T.);
#7466=ORIENTED_EDGE('',*,*,#5545,.T.);
#7467=ORIENTED_EDGE('',*,*,#5544,.F.);
#7468=ORIENTED_EDGE('',*,*,#5546,.T.);
#7469=ORIENTED_EDGE('',*,*,#5547,.T.);
#7470=ORIENTED_EDGE('',*,*,#5548,.F.);
#7471=ORIENTED_EDGE('',*,*,#5547,.F.);
#7472=ORIENTED_EDGE('',*,*,#5548,.T.);
#7473=ORIENTED_EDGE('',*,*,#5549,.T.);
#7474=ORIENTED_EDGE('',*,*,#5550,.F.);
#7475=ORIENTED_EDGE('',*,*,#5549,.F.);
#7476=ORIENTED_EDGE('',*,*,#5545,.F.);
#7477=ORIENTED_EDGE('',*,*,#5550,.T.);
#7478=ORIENTED_EDGE('',*,*,#5551,.F.);
#7479=ORIENTED_EDGE('',*,*,#5552,.T.);
#7480=ORIENTED_EDGE('',*,*,#5539,.T.);
#7481=ORIENTED_EDGE('',*,*,#5540,.T.);
#7482=ORIENTED_EDGE('',*,*,#5552,.F.);
#7483=ORIENTED_EDGE('',*,*,#5551,.T.);
#7484=ORIENTED_EDGE('',*,*,#5553,.F.);
#7485=ORIENTED_EDGE('',*,*,#5553,.T.);
#7486=ORIENTED_EDGE('',*,*,#5554,.T.);
#7487=ORIENTED_EDGE('',*,*,#5546,.F.);
#7488=ORIENTED_EDGE('',*,*,#5554,.F.);
#7841=CYLINDRICAL_SURFACE('',#10048,0.976185);
#7842=CYLINDRICAL_SURFACE('',#10050,0.5);
#7843=CYLINDRICAL_SURFACE('',#10056,0.976185);
#8307=ADVANCED_FACE('',(#1704),#474,.F.);
#8308=ADVANCED_FACE('',(#1705),#7841,.T.);
#8309=ADVANCED_FACE('',(#1706),#7842,.F.);
#8310=ADVANCED_FACE('',(#1707),#495,.F.);
#8311=ADVANCED_FACE('',(#1708,#981),#1233,.T.);
#8312=ADVANCED_FACE('',(#1709),#7843,.T.);
#8313=ADVANCED_FACE('',(#1710,#982),#1234,.T.);
#8314=ADVANCED_FACE('',(#1711),#496,.F.);
#8421=CLOSED_SHELL('',(#8307,#8308,#8309,#8310,#8311,#8312,#8313,#8314));
#10041=AXIS2_PLACEMENT_3D('',#15533,#12669,#12670);
#10042=AXIS2_PLACEMENT_3D('',#15534,#12671,#12672);
#10043=AXIS2_PLACEMENT_3D('',#15537,#12673,#12674);
#10044=AXIS2_PLACEMENT_3D('',#15538,#12675,#12676);
#10045=AXIS2_PLACEMENT_3D('',#15540,#12677,#12678);
#10046=AXIS2_PLACEMENT_3D('',#15542,#12679,#12680);
#10047=AXIS2_PLACEMENT_3D('',#15543,#12681,#12682);
#10048=AXIS2_PLACEMENT_3D('',#15544,#12683,#12684);
#10049=AXIS2_PLACEMENT_3D('',#15547,#12686,#12687);
#10050=AXIS2_PLACEMENT_3D('',#15548,#12688,#12689);
#10051=AXIS2_PLACEMENT_3D('',#15550,#12690,#12691);
#10052=AXIS2_PLACEMENT_3D('',#15553,#12693,#12694);
#10053=AXIS2_PLACEMENT_3D('',#15554,#12695,#12696);
#10054=AXIS2_PLACEMENT_3D('',#15557,#12698,#12699);
#10055=AXIS2_PLACEMENT_3D('',#15558,#12700,#12701);
#10056=AXIS2_PLACEMENT_3D('',#15559,#12702,#12703);
#10057=AXIS2_PLACEMENT_3D('',#15561,#12704,#12705);
#10058=AXIS2_PLACEMENT_3D('',#15563,#12707,#12708);
#10059=AXIS2_PLACEMENT_3D('',#15565,#12709,#12710);
#10060=AXIS2_PLACEMENT_3D('',#15566,#12711,#12712);
#12669=DIRECTION('axis',(0.,0.,1.));
#12670=DIRECTION('refdir',(1.,0.,0.));
#12671=DIRECTION('center_axis',(0.,-1.,0.));
#12672=DIRECTION('ref_axis',(0.,0.,-1.));
#12673=DIRECTION('center_axis',(0.,-1.,0.));
#12674=DIRECTION('ref_axis',(1.,0.,0.));
#12675=DIRECTION('center_axis',(0.,-1.,0.));
#12676=DIRECTION('ref_axis',(1.,0.,0.));
#12677=DIRECTION('center_axis',(1.,0.,1.22464679914735E-16));
#12678=DIRECTION('ref_axis',(-1.22464679914735E-16,0.,1.));
#12679=DIRECTION('center_axis',(0.,1.,0.));
#12680=DIRECTION('ref_axis',(1.,0.,0.));
#12681=DIRECTION('center_axis',(0.,1.,0.));
#12682=DIRECTION('ref_axis',(1.,0.,0.));
#12683=DIRECTION('center_axis',(0.,-1.,0.));
#12684=DIRECTION('ref_axis',(1.,0.,0.));
#12685=DIRECTION('',(0.,1.,0.));
#12686=DIRECTION('center_axis',(0.,-1.,0.));
#12687=DIRECTION('ref_axis',(1.,0.,0.));
#12688=DIRECTION('center_axis',(0.,-1.,0.));
#12689=DIRECTION('ref_axis',(1.,0.,0.));
#12690=DIRECTION('center_axis',(0.,-1.,0.));
#12691=DIRECTION('ref_axis',(1.,0.,0.));
#12692=DIRECTION('',(0.,1.,0.));
#12693=DIRECTION('center_axis',(0.,-1.,0.));
#12694=DIRECTION('ref_axis',(1.,0.,0.));
#12695=DIRECTION('center_axis',(0.,1.,0.));
#12696=DIRECTION('ref_axis',(1.,0.,0.));
#12697=DIRECTION('',(-0.707106781186547,0.707106781186548,-8.65956056235493E-17));
#12698=DIRECTION('center_axis',(0.,-1.,0.));
#12699=DIRECTION('ref_axis',(1.,0.,0.));
#12700=DIRECTION('center_axis',(0.,1.,0.));
#12701=DIRECTION('ref_axis',(0.,0.,1.));
#12702=DIRECTION('center_axis',(0.,-1.,0.));
#12703=DIRECTION('ref_axis',(1.,0.,0.));
#12704=DIRECTION('center_axis',(0.,-1.,0.));
#12705=DIRECTION('ref_axis',(1.,0.,0.));
#12706=DIRECTION('',(0.,1.,0.));
#12707=DIRECTION('center_axis',(0.,-1.,0.));
#12708=DIRECTION('ref_axis',(0.,0.,-1.));
#12709=DIRECTION('center_axis',(0.,-1.,0.));
#12710=DIRECTION('ref_axis',(1.,0.,0.));
#12711=DIRECTION('center_axis',(0.,-1.,0.));
#12712=DIRECTION('ref_axis',(1.,0.,0.));
#12713=DIRECTION('',(0.707106781186547,0.707106781186548,8.65956056235493E-17));
#15533=CARTESIAN_POINT('',(0.,0.,0.));
#15534=CARTESIAN_POINT('Origin',(0.,0.,0.));
#15535=CARTESIAN_POINT('',(-0.976185,-0.246528389340863,-1.19548183562566E-16));
#15536=CARTESIAN_POINT('',(-1.19548183562566E-16,-0.246528389340863,0.976185));
#15537=CARTESIAN_POINT('Origin',(0.,-0.246528389340863,0.));
#15538=CARTESIAN_POINT('Origin',(0.,-0.246528389340863,0.));
#15539=CARTESIAN_POINT('',(-1.19548183562566E-16,0.246528389340863,0.976185));
#15540=CARTESIAN_POINT('Origin',(-1.22464679914735E-16,0.,1.));
#15541=CARTESIAN_POINT('',(-0.976185,0.246528389340863,1.19548183562566E-16));
#15542=CARTESIAN_POINT('Origin',(0.,0.246528389340863,0.));
#15543=CARTESIAN_POINT('Origin',(0.,0.246528389340863,0.));
#15544=CARTESIAN_POINT('Origin',(0.,0.,0.));
#15545=CARTESIAN_POINT('',(-0.976185,0.45,-1.19548183562566E-16));
#15546=CARTESIAN_POINT('',(-0.976185,0.,-1.19548183562566E-16));
#15547=CARTESIAN_POINT('Origin',(0.,0.45,0.));
#15548=CARTESIAN_POINT('Origin',(0.,0.,0.));
#15549=CARTESIAN_POINT('',(-0.5,-0.39,-6.12323399573677E-17));
#15550=CARTESIAN_POINT('Origin',(0.,-0.39,0.));
#15551=CARTESIAN_POINT('',(-0.5,0.39,-6.12323399573677E-17));
#15552=CARTESIAN_POINT('',(-0.5,0.,-6.12323399573677E-17));
#15553=CARTESIAN_POINT('Origin',(0.,0.39,0.));
#15554=CARTESIAN_POINT('Origin',(0.,0.42,0.));
#15555=CARTESIAN_POINT('',(-0.56,0.45,-6.85802207522518E-17));
#15556=CARTESIAN_POINT('',(-0.53,0.42,-6.49062803548097E-17));
#15557=CARTESIAN_POINT('Origin',(0.,0.45,0.));
#15558=CARTESIAN_POINT('Origin',(0.976185,0.45,0.));
#15559=CARTESIAN_POINT('Origin',(0.,0.,0.));
#15560=CARTESIAN_POINT('',(-0.976185,-0.45,-1.19548183562566E-16));
#15561=CARTESIAN_POINT('Origin',(0.,-0.45,0.));
#15562=CARTESIAN_POINT('',(-0.976185,0.,-1.19548183562566E-16));
#15563=CARTESIAN_POINT('Origin',(0.56,-0.45,0.));
#15564=CARTESIAN_POINT('',(-0.56,-0.45,-6.85802207522518E-17));
#15565=CARTESIAN_POINT('Origin',(0.,-0.45,0.));
#15566=CARTESIAN_POINT('Origin',(0.,-0.42,0.));
#15567=CARTESIAN_POINT('',(-0.53,-0.42,-6.49062803548097E-17));
#16207=UNCERTAINTY_MEASURE_WITH_UNIT(LENGTH_MEASURE(0.001),#16282,
'DISTANCE_ACCURACY_VALUE',
'Maximum model space distance between geometric entities at asserted c
onnectivities');
#16212=UNCERTAINTY_MEASURE_WITH_UNIT(LENGTH_MEASURE(0.001),#16282,
'DISTANCE_ACCURACY_VALUE',
'Maximum model space distance between geometric entities at asserted c
onnectivities');
#16276=(
GEOMETRIC_REPRESENTATION_CONTEXT(3)
GLOBAL_UNCERTAINTY_ASSIGNED_CONTEXT((#16207))
GLOBAL_UNIT_ASSIGNED_CONTEXT((#16282,#16284,#16285))
REPRESENTATION_CONTEXT('','3D')
);
#16281=(
GEOMETRIC_REPRESENTATION_CONTEXT(3)
GLOBAL_UNCERTAINTY_ASSIGNED_CONTEXT((#16212))
GLOBAL_UNIT_ASSIGNED_CONTEXT((#16282,#16284,#16285))
REPRESENTATION_CONTEXT('','3D')
);
#16282=(
LENGTH_UNIT()
NAMED_UNIT(*)
SI_UNIT(.CENTI.,.METRE.)
);
#16284=(
NAMED_UNIT(*)
PLANE_ANGLE_UNIT()
SI_UNIT($,.RADIAN.)
);
#16285=(
NAMED_UNIT(*)
SI_UNIT($,.STERADIAN.)
SOLID_ANGLE_UNIT()
);
#16349=SHAPE_DEFINITION_REPRESENTATION(#16483,#16582);
#16483=PRODUCT_DEFINITION_SHAPE('',$,#16651);
#16582=SHAPE_REPRESENTATION('',(#10041),#16276);
#16587=PRODUCT_DEFINITION_CONTEXT('part definition',#16793,'design');
#16651=PRODUCT_DEFINITION('Inner ring (1)','Inner ring (1)',#16719,#16587);
#16719=PRODUCT_DEFINITION_FORMATION('',$,#16858);
#16793=APPLICATION_CONTEXT(
'Core Data for Automotive Mechanical Design Process');
#16794=PRODUCT_CONTEXT('part definition',#16793,'mechanical');
#16858=PRODUCT('Inner ring (1)','Inner ring (1)','Inner ring (1)',(#16794));
#16926=COLOUR_RGB('Grey',0.48,0.52,0.57);
#16927=FILL_AREA_STYLE_COLOUR('',#16926);
#16928=FILL_AREA_STYLE('',(#16927));
#16929=SURFACE_STYLE_FILL_AREA(#16928);
#16930=SURFACE_SIDE_STYLE('',(#16929));
#16931=SURFACE_STYLE_USAGE(.BOTH.,#16930);
#16932=PRESENTATION_STYLE_ASSIGNMENT((#16931));
ENDSEC;
END-ISO-10303-21;
